ISO-10303-21;
HEADER;
/* Generated by software containing ST-Developer
 * from STEP Tools, Inc. (www.steptools.com) 
 */

FILE_DESCRIPTION(
/* description */ (''),
/* implementation_level */ '2;1');

FILE_NAME(
/* name */ 'DIN7603 A10x14x1 Copper Washer.step',
/* time_stamp */ '2026-10-15T14:25:16-07:00',
/* author */ (''),
/* organization */ (''),
/* preprocessor_version */ 'ST-DEVELOPER v20.2',
/* originating_system */ 'Autodesk Translation Framework v15.15.0.0',
/* authorisation */ '');

FILE_SCHEMA (('AUTOMOTIVE_DESIGN { 1 0 10303 214 3 1 1 }'));
ENDSEC;

DATA;
#10=MECHANICAL_DESIGN_GEOMETRIC_PRESENTATION_REPRESENTATION('',(#332),#86429);
#296=SHAPE_REPRESENTATION_RELATIONSHIP('SRR','None',#86511,#314);
#314=ADVANCED_BREP_SHAPE_REPRESENTATION('',(#350),#86420);
#332=STYLED_ITEM('',(#86610),#350);
#350=MANIFOLD_SOLID_BREP('Body1',#15622);
#1314=CONICAL_SURFACE('',#16949,0.515,0.785398163397449);
#1315=CONICAL_SURFACE('',#16954,0.695,0.785398163397443);
#1316=CONICAL_SURFACE('',#16958,0.695,0.785398163397443);
#1317=CONICAL_SURFACE('',#16962,0.515,0.785398163397448);
#1530=CYLINDRICAL_SURFACE('',#16956,0.7);
#1531=CYLINDRICAL_SURFACE('',#16964,0.51);
#1721=FACE_BOUND('',#4078,.T.);
#1722=FACE_BOUND('',#4083,.T.);
#2253=CIRCLE('',#16950,0.51);
#2254=CIRCLE('',#16951,0.52);
#2255=CIRCLE('',#16953,0.69);
#2256=CIRCLE('',#16955,0.7);
#2257=CIRCLE('',#16957,0.7);
#2258=CIRCLE('',#16959,0.69);
#2259=CIRCLE('',#16961,0.52);
#2260=CIRCLE('',#16963,0.51);
#3085=FACE_OUTER_BOUND('',#4076,.T.);
#3086=FACE_OUTER_BOUND('',#4077,.T.);
#3087=FACE_OUTER_BOUND('',#4079,.T.);
#3088=FACE_OUTER_BOUND('',#4080,.T.);
#3089=FACE_OUTER_BOUND('',#4081,.T.);
#3090=FACE_OUTER_BOUND('',#4082,.T.);
#3091=FACE_OUTER_BOUND('',#4084,.T.);
#3092=FACE_OUTER_BOUND('',#4085,.T.);
#4076=EDGE_LOOP('',(#13501,#13502,#13503,#13504));
#4077=EDGE_LOOP('',(#13505));
#4078=EDGE_LOOP('',(#13506));
#4079=EDGE_LOOP('',(#13507,#13508,#13509,#13510));
#4080=EDGE_LOOP('',(#13511,#13512,#13513,#13514));
#4081=EDGE_LOOP('',(#13515,#13516,#13517,#13518));
#4082=EDGE_LOOP('',(#13519));
#4083=EDGE_LOOP('',(#13520));
#4084=EDGE_LOOP('',(#13521,#13522,#13523,#13524));
#4085=EDGE_LOOP('',(#13525,#13526,#13527,#13528));
#5006=LINE('',#66312,#5866);
#5007=LINE('',#66320,#5867);
#5008=LINE('',#66324,#5868);
#5009=LINE('',#66327,#5869);
#5010=LINE('',#66335,#5870);
#5011=LINE('',#66337,#5871);
#5866=VECTOR('',#20253,0.515);
#5867=VECTOR('',#20264,0.695);
#5868=VECTOR('',#20269,0.7);
#5869=VECTOR('',#20272,0.695);
#5870=VECTOR('',#20283,0.515);
#5871=VECTOR('',#20286,0.51);
#7201=VERTEX_POINT('',#66309);
#7202=VERTEX_POINT('',#66311);
#7203=VERTEX_POINT('',#66315);
#7204=VERTEX_POINT('',#66318);
#7205=VERTEX_POINT('',#66322);
#7206=VERTEX_POINT('',#66326);
#7207=VERTEX_POINT('',#66330);
#7208=VERTEX_POINT('',#66333);
#9372=EDGE_CURVE('',#7201,#7201,#2253,.T.);
#9373=EDGE_CURVE('',#7201,#7202,#5006,.T.);
#9374=EDGE_CURVE('',#7202,#7202,#2254,.T.);
#9375=EDGE_CURVE('',#7203,#7203,#2255,.T.);
#9376=EDGE_CURVE('',#7204,#7204,#2256,.T.);
#9377=EDGE_CURVE('',#7204,#7203,#5007,.T.);
#9378=EDGE_CURVE('',#7205,#7205,#2257,.T.);
#9379=EDGE_CURVE('',#7205,#7204,#5008,.T.);
#9380=EDGE_CURVE('',#7205,#7206,#5009,.T.);
#9381=EDGE_CURVE('',#7206,#7206,#2258,.T.);
#9382=EDGE_CURVE('',#7207,#7207,#2259,.T.);
#9383=EDGE_CURVE('',#7208,#7208,#2260,.T.);
#9384=EDGE_CURVE('',#7208,#7207,#5010,.T.);
#9385=EDGE_CURVE('',#7201,#7208,#5011,.T.);
#13501=ORIENTED_EDGE('',*,*,#9372,.T.);
#13502=ORIENTED_EDGE('',*,*,#9373,.T.);
#13503=ORIENTED_EDGE('',*,*,#9374,.F.);
#13504=ORIENTED_EDGE('',*,*,#9373,.F.);
#13505=ORIENTED_EDGE('',*,*,#9375,.F.);
#13506=ORIENTED_EDGE('',*,*,#9374,.T.);
#13507=ORIENTED_EDGE('',*,*,#9376,.F.);
#13508=ORIENTED_EDGE('',*,*,#9377,.T.);
#13509=ORIENTED_EDGE('',*,*,#9375,.T.);
#13510=ORIENTED_EDGE('',*,*,#9377,.F.);
#13511=ORIENTED_EDGE('',*,*,#9378,.F.);
#13512=ORIENTED_EDGE('',*,*,#9379,.T.);
#13513=ORIENTED_EDGE('',*,*,#9376,.T.);
#13514=ORIENTED_EDGE('',*,*,#9379,.F.);
#13515=ORIENTED_EDGE('',*,*,#9378,.T.);
#13516=ORIENTED_EDGE('',*,*,#9380,.T.);
#13517=ORIENTED_EDGE('',*,*,#9381,.F.);
#13518=ORIENTED_EDGE('',*,*,#9380,.F.);
#13519=ORIENTED_EDGE('',*,*,#9381,.T.);
#13520=ORIENTED_EDGE('',*,*,#9382,.F.);
#13521=ORIENTED_EDGE('',*,*,#9383,.F.);
#13522=ORIENTED_EDGE('',*,*,#9384,.T.);
#13523=ORIENTED_EDGE('',*,*,#9382,.T.);
#13524=ORIENTED_EDGE('',*,*,#9384,.F.);
#13525=ORIENTED_EDGE('',*,*,#9372,.F.);
#13526=ORIENTED_EDGE('',*,*,#9385,.T.);
#13527=ORIENTED_EDGE('',*,*,#9383,.T.);
#13528=ORIENTED_EDGE('',*,*,#9385,.F.);
#14686=PLANE('',#16952);
#14687=PLANE('',#16960);
#15441=ADVANCED_FACE('',(#3085),#1314,.F.);
#15442=ADVANCED_FACE('',(#3086,#1721),#14686,.T.);
#15443=ADVANCED_FACE('',(#3087),#1315,.T.);
#15444=ADVANCED_FACE('',(#3088),#1530,.T.);
#15445=ADVANCED_FACE('',(#3089),#1316,.T.);
#15446=ADVANCED_FACE('',(#3090,#1722),#14687,.T.);
#15447=ADVANCED_FACE('',(#3091),#1317,.F.);
#15448=ADVANCED_FACE('',(#3092),#1531,.F.);
#15622=CLOSED_SHELL('',(#15441,#15442,#15443,#15444,#15445,#15446,#15447,
#15448));
#16948=AXIS2_PLACEMENT_3D('',#66307,#20247,#20248);
#16949=AXIS2_PLACEMENT_3D('',#66308,#20249,#20250);
#16950=AXIS2_PLACEMENT_3D('',#66310,#20251,#20252);
#16951=AXIS2_PLACEMENT_3D('',#66313,#20254,#20255);
#16952=AXIS2_PLACEMENT_3D('',#66314,#20256,#20257);
#16953=AXIS2_PLACEMENT_3D('',#66316,#20258,#20259);
#16954=AXIS2_PLACEMENT_3D('',#66317,#20260,#20261);
#16955=AXIS2_PLACEMENT_3D('',#66319,#20262,#20263);
#16956=AXIS2_PLACEMENT_3D('',#66321,#20265,#20266);
#16957=AXIS2_PLACEMENT_3D('',#66323,#20267,#20268);
#16958=AXIS2_PLACEMENT_3D('',#66325,#20270,#20271);
#16959=AXIS2_PLACEMENT_3D('',#66328,#20273,#20274);
#16960=AXIS2_PLACEMENT_3D('',#66329,#20275,#20276);
#16961=AXIS2_PLACEMENT_3D('',#66331,#20277,#20278);
#16962=AXIS2_PLACEMENT_3D('',#66332,#20279,#20280);
#16963=AXIS2_PLACEMENT_3D('',#66334,#20281,#20282);
#16964=AXIS2_PLACEMENT_3D('',#66336,#20284,#20285);
#20247=DIRECTION('axis',(0.,0.,1.));
#20248=DIRECTION('refdir',(1.,0.,0.));
#20249=DIRECTION('center_axis',(0.,0.,-1.));
#20250=DIRECTION('ref_axis',(1.,0.,0.));
#20251=DIRECTION('center_axis',(0.,0.,1.));
#20252=DIRECTION('ref_axis',(1.,0.,0.));
#20253=DIRECTION('',(-0.707106781186548,8.65956056235494E-17,-0.707106781186547));
#20254=DIRECTION('center_axis',(0.,0.,1.));
#20255=DIRECTION('ref_axis',(1.,0.,0.));
#20256=DIRECTION('center_axis',(0.,0.,-1.));
#20257=DIRECTION('ref_axis',(-1.,0.,0.));
#20258=DIRECTION('center_axis',(0.,0.,1.));
#20259=DIRECTION('ref_axis',(1.,0.,0.));
#20260=DIRECTION('center_axis',(0.,0.,1.));
#20261=DIRECTION('ref_axis',(1.,0.,0.));
#20262=DIRECTION('center_axis',(0.,0.,1.));
#20263=DIRECTION('ref_axis',(1.,0.,0.));
#20264=DIRECTION('',(0.707106781186544,8.65956056235489E-17,-0.707106781186551));
#20265=DIRECTION('center_axis',(0.,0.,1.));
#20266=DIRECTION('ref_axis',(1.,0.,0.));
#20267=DIRECTION('center_axis',(0.,0.,1.));
#20268=DIRECTION('ref_axis',(1.,0.,0.));
#20269=DIRECTION('',(0.,0.,-1.));
#20270=DIRECTION('center_axis',(0.,0.,-1.));
#20271=DIRECTION('ref_axis',(1.,0.,0.));
#20272=DIRECTION('',(0.707106781186544,-8.65956056235489E-17,0.707106781186551));
#20273=DIRECTION('center_axis',(0.,0.,1.));
#20274=DIRECTION('ref_axis',(1.,0.,0.));
#20275=DIRECTION('center_axis',(0.,0.,1.));
#20276=DIRECTION('ref_axis',(1.,0.,0.));
#20277=DIRECTION('center_axis',(0.,0.,1.));
#20278=DIRECTION('ref_axis',(1.,0.,0.));
#20279=DIRECTION('center_axis',(0.,0.,1.));
#20280=DIRECTION('ref_axis',(1.,0.,0.));
#20281=DIRECTION('center_axis',(0.,0.,1.));
#20282=DIRECTION('ref_axis',(1.,0.,0.));
#20283=DIRECTION('',(-0.707106781186547,-8.65956056235493E-17,0.707106781186548));
#20284=DIRECTION('center_axis',(0.,0.,1.));
#20285=DIRECTION('ref_axis',(1.,0.,0.));
#20286=DIRECTION('',(0.,0.,1.));
#66307=CARTESIAN_POINT('',(0.,0.,0.));
#66308=CARTESIAN_POINT('Origin',(0.,0.,0.005));
#66309=CARTESIAN_POINT('',(-0.51,-6.2456986756515E-17,0.01));
#66310=CARTESIAN_POINT('Origin',(0.,0.,0.01));
#66311=CARTESIAN_POINT('',(-0.52,-6.36816335556624E-17,0.));
#66312=CARTESIAN_POINT('',(-0.515,6.30693101560887E-17,0.005));
#66313=CARTESIAN_POINT('Origin',(0.,0.,0.));
#66314=CARTESIAN_POINT('Origin',(0.69,0.,0.));
#66315=CARTESIAN_POINT('',(-0.69,-8.45006291411674E-17,-2.60208521396521E-17));
#66316=CARTESIAN_POINT('Origin',(0.,0.,0.));
#66317=CARTESIAN_POINT('Origin',(0.,0.,0.005));
#66318=CARTESIAN_POINT('',(-0.7,-8.57252759403147E-17,0.00999999999999998));
#66319=CARTESIAN_POINT('Origin',(0.,0.,0.01));
#66320=CARTESIAN_POINT('',(-0.695,-8.5112952540741E-17,0.005));
#66321=CARTESIAN_POINT('Origin',(0.,0.,0.05));
#66322=CARTESIAN_POINT('',(-0.7,-8.57252759403147E-17,0.09));
#66323=CARTESIAN_POINT('Origin',(0.,0.,0.09));
#66324=CARTESIAN_POINT('',(-0.7,-8.57252759403147E-17,0.05));
#66325=CARTESIAN_POINT('Origin',(0.,0.,0.095));
#66326=CARTESIAN_POINT('',(-0.69,-8.45006291411674E-17,0.1));
#66327=CARTESIAN_POINT('',(-0.695,8.5112952540741E-17,0.095));
#66328=CARTESIAN_POINT('Origin',(0.,0.,0.1));
#66329=CARTESIAN_POINT('Origin',(0.52,0.,0.1));
#66330=CARTESIAN_POINT('',(-0.52,-6.36816335556624E-17,0.1));
#66331=CARTESIAN_POINT('Origin',(0.,0.,0.1));
#66332=CARTESIAN_POINT('Origin',(0.,0.,0.095));
#66333=CARTESIAN_POINT('',(-0.51,-6.2456986756515E-17,0.09));
#66334=CARTESIAN_POINT('Origin',(0.,0.,0.09));
#66335=CARTESIAN_POINT('',(-0.515,-6.30693101560887E-17,0.095));
#66336=CARTESIAN_POINT('Origin',(0.,0.,0.05));
#66337=CARTESIAN_POINT('',(-0.51,-6.2456986756515E-17,0.05));
#86400=UNCERTAINTY_MEASURE_WITH_UNIT(LENGTH_MEASURE(0.001),#86430,
'DISTANCE_ACCURACY_VALUE',
'Maximum model space distance between geometric entities at asserted c
onnectivities');
#86409=UNCERTAINTY_MEASURE_WITH_UNIT(LENGTH_MEASURE(0.001),#86430,
'DISTANCE_ACCURACY_VALUE',
'Maximum model space distance between geometric entities at asserted c
onnectivities');
#86420=(
GEOMETRIC_REPRESENTATION_CONTEXT(3)
GLOBAL_UNCERTAINTY_ASSIGNED_CONTEXT((#86400))
GLOBAL_UNIT_ASSIGNED_CONTEXT((#86430,#86432,#86433))
REPRESENTATION_CONTEXT('','3D')
);
#86429=(
GEOMETRIC_REPRESENTATION_CONTEXT(3)
GLOBAL_UNCERTAINTY_ASSIGNED_CONTEXT((#86409))
GLOBAL_UNIT_ASSIGNED_CONTEXT((#86430,#86432,#86433))
REPRESENTATION_CONTEXT('','3D')
);
#86430=(
LENGTH_UNIT()
NAMED_UNIT(*)
SI_UNIT(.CENTI.,.METRE.)
);
#86432=(
NAMED_UNIT(*)
PLANE_ANGLE_UNIT()
SI_UNIT($,.RADIAN.)
);
#86433=(
NAMED_UNIT(*)
SI_UNIT($,.STERADIAN.)
SOLID_ANGLE_UNIT()
);
#86444=SHAPE_DEFINITION_REPRESENTATION(#86463,#86511);
#86463=PRODUCT_DEFINITION_SHAPE('',$,#86531);
#86511=SHAPE_REPRESENTATION('',(#16948),#86420);
#86520=PRODUCT_DEFINITION_CONTEXT('part definition',#86579,'design');
#86531=PRODUCT_DEFINITION('DIN7603 A10x14x1 Copper Washer',
'DIN7603 A10x14x1 Copper Washer',#86550,#86520);
#86550=PRODUCT_DEFINITION_FORMATION('',$,#86591);
#86579=APPLICATION_CONTEXT(
'Core Data for Automotive Mechanical Design Process');
#86580=PRODUCT_CONTEXT('part definition',#86579,'mechanical');
#86591=PRODUCT('DIN7603 A10x14x1 Copper Washer',
'DIN7603 A10x14x1 Copper Washer',$,(#86580));
#86610=PRESENTATION_STYLE_ASSIGNMENT((#86628));
#86628=SURFACE_STYLE_USAGE(.BOTH.,#86646);
#86646=SURFACE_SIDE_STYLE('',(#86664));
#86664=SURFACE_STYLE_FILL_AREA(#86682);
#86682=FILL_AREA_STYLE('Opaque(200,128,82)',(#86700));
#86700=FILL_AREA_STYLE_COLOUR('Opaque(200,128,82)',#86718);
#86718=COLOUR_RGB('Opaque(200,128,82)', 0.40784314, 0.44705882, 0.49803922);
ENDSEC;
END-ISO-10303-21;
